ISO-10303-21;
HEADER;
/* Generated by software containing ST-Developer
 * from STEP Tools, Inc. (www.steptools.com) 
 */

FILE_DESCRIPTION(
/* description */ ('Ratchet and pawl hand winch drum'),
/* implementation_level */ '2;1');

FILE_NAME(
/* name */ 'Socket Set Screw - M5x8.step',
/* time_stamp */ '2026-10-27T12:42:58-07:00',
/* author */ (''),
/* organization */ (''),
/* preprocessor_version */ 'ST-DEVELOPER v20.2',
/* originating_system */ 'Autodesk Translation Framework v15.17.0.0',
/* authorisation */ '');

FILE_SCHEMA (('AUTOMOTIVE_DESIGN { 1 0 10303 214 3 1 1 }'));
ENDSEC;

DATA;
#10=MECHANICAL_DESIGN_GEOMETRIC_PRESENTATION_REPRESENTATION('',(#421),#11801);
#17=CONICAL_SURFACE('',#7253,0.235,0.785398163397448);
#18=CONICAL_SURFACE('',#7257,0.2125,0.785398163397448);
#352=SHAPE_REPRESENTATION_RELATIONSHIP('SRR','None',#11980,#386);
#386=ADVANCED_BREP_SHAPE_REPRESENTATION('',(#454),#11797);
#421=STYLED_ITEM('',(#12220),#454);
#454=MANIFOLD_SOLID_BREP('Body1',#6300);
#597=FACE_BOUND('',#1665,.T.);
#815=PLANE('',#7244);
#816=PLANE('',#7245);
#817=PLANE('',#7246);
#818=PLANE('',#7247);
#819=PLANE('',#7248);
#820=PLANE('',#7249);
#821=PLANE('',#7250);
#822=PLANE('',#7251);
#823=PLANE('',#7259);
#1160=FACE_OUTER_BOUND('',#1657,.T.);
#1161=FACE_OUTER_BOUND('',#1658,.T.);
#1162=FACE_OUTER_BOUND('',#1659,.T.);
#1163=FACE_OUTER_BOUND('',#1660,.T.);
#1164=FACE_OUTER_BOUND('',#1661,.T.);
#1165=FACE_OUTER_BOUND('',#1662,.T.);
#1166=FACE_OUTER_BOUND('',#1663,.T.);
#1167=FACE_OUTER_BOUND('',#1664,.T.);
#1168=FACE_OUTER_BOUND('',#1666,.T.);
#1169=FACE_OUTER_BOUND('',#1667,.T.);
#1170=FACE_OUTER_BOUND('',#1668,.T.);
#1171=FACE_OUTER_BOUND('',#1669,.T.);
#1657=EDGE_LOOP('',(#5663,#5664,#5665,#5666));
#1658=EDGE_LOOP('',(#5667,#5668,#5669,#5670));
#1659=EDGE_LOOP('',(#5671,#5672,#5673,#5674));
#1660=EDGE_LOOP('',(#5675,#5676,#5677,#5678));
#1661=EDGE_LOOP('',(#5679,#5680,#5681,#5682));
#1662=EDGE_LOOP('',(#5683,#5684,#5685,#5686));
#1663=EDGE_LOOP('',(#5687,#5688,#5689,#5690,#5691,#5692));
#1664=EDGE_LOOP('',(#5693));
#1665=EDGE_LOOP('',(#5694,#5695,#5696,#5697,#5698,#5699));
#1666=EDGE_LOOP('',(#5700,#5701,#5702,#5703));
#1667=EDGE_LOOP('',(#5704,#5705,#5706,#5707));
#1668=EDGE_LOOP('',(#5708,#5709,#5710,#5711));
#1669=EDGE_LOOP('',(#5712));
#2152=LINE('',#11509,#2663);
#2153=LINE('',#11511,#2664);
#2154=LINE('',#11513,#2665);
#2155=LINE('',#11514,#2666);
#2156=LINE('',#11517,#2667);
#2157=LINE('',#11519,#2668);
#2158=LINE('',#11520,#2669);
#2159=LINE('',#11523,#2670);
#2160=LINE('',#11525,#2671);
#2161=LINE('',#11526,#2672);
#2162=LINE('',#11529,#2673);
#2163=LINE('',#11531,#2674);
#2164=LINE('',#11532,#2675);
#2165=LINE('',#11535,#2676);
#2166=LINE('',#11537,#2677);
#2167=LINE('',#11538,#2678);
#2168=LINE('',#11540,#2679);
#2169=LINE('',#11541,#2680);
#2170=LINE('',#11549,#2681);
#2171=LINE('',#11553,#2682);
#2172=LINE('',#11557,#2683);
#2663=VECTOR('',#8945,1.);
#2664=VECTOR('',#8946,1.);
#2665=VECTOR('',#8947,1.);
#2666=VECTOR('',#8948,1.);
#2667=VECTOR('',#8951,1.);
#2668=VECTOR('',#8952,1.);
#2669=VECTOR('',#8953,1.);
#2670=VECTOR('',#8956,1.);
#2671=VECTOR('',#8957,1.);
#2672=VECTOR('',#8958,1.);
#2673=VECTOR('',#8961,1.);
#2674=VECTOR('',#8962,1.);
#2675=VECTOR('',#8963,1.);
#2676=VECTOR('',#8966,1.);
#2677=VECTOR('',#8967,1.);
#2678=VECTOR('',#8968,1.);
#2679=VECTOR('',#8971,1.);
#2680=VECTOR('',#8972,1.);
#2681=VECTOR('',#8983,0.235);
#2682=VECTOR('',#8988,0.25);
#2683=VECTOR('',#8993,0.2125);
#2926=CIRCLE('',#7252,0.22);
#2927=CIRCLE('',#7254,0.24505);
#2928=CIRCLE('',#7256,0.24505);
#2929=CIRCLE('',#7258,0.175);
#3421=VERTEX_POINT('',#11507);
#3422=VERTEX_POINT('',#11508);
#3423=VERTEX_POINT('',#11510);
#3424=VERTEX_POINT('',#11512);
#3425=VERTEX_POINT('',#11516);
#3426=VERTEX_POINT('',#11518);
#3427=VERTEX_POINT('',#11522);
#3428=VERTEX_POINT('',#11524);
#3429=VERTEX_POINT('',#11528);
#3430=VERTEX_POINT('',#11530);
#3431=VERTEX_POINT('',#11534);
#3432=VERTEX_POINT('',#11536);
#3433=VERTEX_POINT('',#11544);
#3434=VERTEX_POINT('',#11547);
#3435=VERTEX_POINT('',#11551);
#3436=VERTEX_POINT('',#11555);
#4175=EDGE_CURVE('',#3421,#3422,#2152,.T.);
#4176=EDGE_CURVE('',#3421,#3423,#2153,.T.);
#4177=EDGE_CURVE('',#3423,#3424,#2154,.T.);
#4178=EDGE_CURVE('',#3422,#3424,#2155,.T.);
#4179=EDGE_CURVE('',#3425,#3421,#2156,.T.);
#4180=EDGE_CURVE('',#3425,#3426,#2157,.T.);
#4181=EDGE_CURVE('',#3426,#3423,#2158,.T.);
#4182=EDGE_CURVE('',#3427,#3425,#2159,.T.);
#4183=EDGE_CURVE('',#3427,#3428,#2160,.T.);
#4184=EDGE_CURVE('',#3428,#3426,#2161,.T.);
#4185=EDGE_CURVE('',#3429,#3427,#2162,.T.);
#4186=EDGE_CURVE('',#3429,#3430,#2163,.T.);
#4187=EDGE_CURVE('',#3430,#3428,#2164,.T.);
#4188=EDGE_CURVE('',#3431,#3429,#2165,.T.);
#4189=EDGE_CURVE('',#3431,#3432,#2166,.T.);
#4190=EDGE_CURVE('',#3432,#3430,#2167,.T.);
#4191=EDGE_CURVE('',#3422,#3431,#2168,.T.);
#4192=EDGE_CURVE('',#3424,#3432,#2169,.T.);
#4193=EDGE_CURVE('',#3433,#3433,#2926,.T.);
#4194=EDGE_CURVE('',#3434,#3434,#2927,.T.);
#4195=EDGE_CURVE('',#3434,#3433,#2170,.T.);
#4196=EDGE_CURVE('',#3435,#3435,#2928,.F.);
#4197=EDGE_CURVE('',#3435,#3434,#2171,.T.);
#4198=EDGE_CURVE('',#3436,#3436,#2929,.T.);
#4199=EDGE_CURVE('',#3436,#3435,#2172,.T.);
#5663=ORIENTED_EDGE('',*,*,#4175,.F.);
#5664=ORIENTED_EDGE('',*,*,#4176,.T.);
#5665=ORIENTED_EDGE('',*,*,#4177,.T.);
#5666=ORIENTED_EDGE('',*,*,#4178,.F.);
#5667=ORIENTED_EDGE('',*,*,#4179,.F.);
#5668=ORIENTED_EDGE('',*,*,#4180,.T.);
#5669=ORIENTED_EDGE('',*,*,#4181,.T.);
#5670=ORIENTED_EDGE('',*,*,#4176,.F.);
#5671=ORIENTED_EDGE('',*,*,#4182,.F.);
#5672=ORIENTED_EDGE('',*,*,#4183,.T.);
#5673=ORIENTED_EDGE('',*,*,#4184,.T.);
#5674=ORIENTED_EDGE('',*,*,#4180,.F.);
#5675=ORIENTED_EDGE('',*,*,#4185,.F.);
#5676=ORIENTED_EDGE('',*,*,#4186,.T.);
#5677=ORIENTED_EDGE('',*,*,#4187,.T.);
#5678=ORIENTED_EDGE('',*,*,#4183,.F.);
#5679=ORIENTED_EDGE('',*,*,#4188,.F.);
#5680=ORIENTED_EDGE('',*,*,#4189,.T.);
#5681=ORIENTED_EDGE('',*,*,#4190,.T.);
#5682=ORIENTED_EDGE('',*,*,#4186,.F.);
#5683=ORIENTED_EDGE('',*,*,#4191,.F.);
#5684=ORIENTED_EDGE('',*,*,#4178,.T.);
#5685=ORIENTED_EDGE('',*,*,#4192,.T.);
#5686=ORIENTED_EDGE('',*,*,#4189,.F.);
#5687=ORIENTED_EDGE('',*,*,#4192,.F.);
#5688=ORIENTED_EDGE('',*,*,#4177,.F.);
#5689=ORIENTED_EDGE('',*,*,#4181,.F.);
#5690=ORIENTED_EDGE('',*,*,#4184,.F.);
#5691=ORIENTED_EDGE('',*,*,#4187,.F.);
#5692=ORIENTED_EDGE('',*,*,#4190,.F.);
#5693=ORIENTED_EDGE('',*,*,#4193,.F.);
#5694=ORIENTED_EDGE('',*,*,#4175,.T.);
#5695=ORIENTED_EDGE('',*,*,#4191,.T.);
#5696=ORIENTED_EDGE('',*,*,#4188,.T.);
#5697=ORIENTED_EDGE('',*,*,#4185,.T.);
#5698=ORIENTED_EDGE('',*,*,#4182,.T.);
#5699=ORIENTED_EDGE('',*,*,#4179,.T.);
#5700=ORIENTED_EDGE('',*,*,#4194,.F.);
#5701=ORIENTED_EDGE('',*,*,#4195,.T.);
#5702=ORIENTED_EDGE('',*,*,#4193,.T.);
#5703=ORIENTED_EDGE('',*,*,#4195,.F.);
#5704=ORIENTED_EDGE('',*,*,#4196,.F.);
#5705=ORIENTED_EDGE('',*,*,#4197,.T.);
#5706=ORIENTED_EDGE('',*,*,#4194,.T.);
#5707=ORIENTED_EDGE('',*,*,#4197,.F.);
#5708=ORIENTED_EDGE('',*,*,#4198,.F.);
#5709=ORIENTED_EDGE('',*,*,#4199,.T.);
#5710=ORIENTED_EDGE('',*,*,#4196,.T.);
#5711=ORIENTED_EDGE('',*,*,#4199,.F.);
#5712=ORIENTED_EDGE('',*,*,#4198,.T.);
#5905=CYLINDRICAL_SURFACE('',#7255,0.24505);
#6230=ADVANCED_FACE('',(#1160),#815,.F.);
#6231=ADVANCED_FACE('',(#1161),#816,.F.);
#6232=ADVANCED_FACE('',(#1162),#817,.F.);
#6233=ADVANCED_FACE('',(#1163),#818,.F.);
#6234=ADVANCED_FACE('',(#1164),#819,.F.);
#6235=ADVANCED_FACE('',(#1165),#820,.F.);
#6236=ADVANCED_FACE('',(#1166),#821,.F.);
#6237=ADVANCED_FACE('',(#1167,#597),#822,.T.);
#6238=ADVANCED_FACE('',(#1168),#17,.T.);
#6239=ADVANCED_FACE('',(#1169),#5905,.T.);
#6240=ADVANCED_FACE('',(#1170),#18,.T.);
#6241=ADVANCED_FACE('',(#1171),#823,.T.);
#6300=CLOSED_SHELL('',(#6230,#6231,#6232,#6233,#6234,#6235,#6236,#6237,
#6238,#6239,#6240,#6241));
#7243=AXIS2_PLACEMENT_3D('',#11505,#8941,#8942);
#7244=AXIS2_PLACEMENT_3D('',#11506,#8943,#8944);
#7245=AXIS2_PLACEMENT_3D('',#11515,#8949,#8950);
#7246=AXIS2_PLACEMENT_3D('',#11521,#8954,#8955);
#7247=AXIS2_PLACEMENT_3D('',#11527,#8959,#8960);
#7248=AXIS2_PLACEMENT_3D('',#11533,#8964,#8965);
#7249=AXIS2_PLACEMENT_3D('',#11539,#8969,#8970);
#7250=AXIS2_PLACEMENT_3D('',#11542,#8973,#8974);
#7251=AXIS2_PLACEMENT_3D('',#11543,#8975,#8976);
#7252=AXIS2_PLACEMENT_3D('',#11545,#8977,#8978);
#7253=AXIS2_PLACEMENT_3D('',#11546,#8979,#8980);
#7254=AXIS2_PLACEMENT_3D('',#11548,#8981,#8982);
#7255=AXIS2_PLACEMENT_3D('',#11550,#8984,#8985);
#7256=AXIS2_PLACEMENT_3D('',#11552,#8986,#8987);
#7257=AXIS2_PLACEMENT_3D('',#11554,#8989,#8990);
#7258=AXIS2_PLACEMENT_3D('',#11556,#8991,#8992);
#7259=AXIS2_PLACEMENT_3D('',#11558,#8994,#8995);
#8941=DIRECTION('axis',(0.,0.,1.));
#8942=DIRECTION('refdir',(1.,0.,0.));
#8943=DIRECTION('center_axis',(0.866025403784439,0.,-0.5));
#8944=DIRECTION('ref_axis',(0.5,0.,0.866025403784439));
#8945=DIRECTION('',(0.5,0.,0.866025403784439));
#8946=DIRECTION('',(0.,-1.,0.));
#8947=DIRECTION('',(0.5,0.,0.866025403784439));
#8948=DIRECTION('',(0.,-1.,0.));
#8949=DIRECTION('center_axis',(1.92296268638356E-16,0.,-1.));
#8950=DIRECTION('ref_axis',(1.,0.,1.92296268638356E-16));
#8951=DIRECTION('',(1.,0.,1.92296268638356E-16));
#8952=DIRECTION('',(0.,-1.,0.));
#8953=DIRECTION('',(1.,0.,1.92296268638356E-16));
#8954=DIRECTION('center_axis',(-0.866025403784439,0.,-0.5));
#8955=DIRECTION('ref_axis',(0.5,0.,-0.866025403784439));
#8956=DIRECTION('',(0.5,0.,-0.866025403784439));
#8957=DIRECTION('',(0.,-1.,0.));
#8958=DIRECTION('',(0.5,0.,-0.866025403784438));
#8959=DIRECTION('center_axis',(-0.866025403784439,0.,0.5));
#8960=DIRECTION('ref_axis',(-0.5,0.,-0.866025403784439));
#8961=DIRECTION('',(-0.5,0.,-0.866025403784439));
#8962=DIRECTION('',(0.,-1.,0.));
#8963=DIRECTION('',(-0.5,0.,-0.866025403784439));
#8964=DIRECTION('center_axis',(-1.92296268638356E-16,0.,1.));
#8965=DIRECTION('ref_axis',(-1.,0.,-1.92296268638356E-16));
#8966=DIRECTION('',(-1.,0.,-1.92296268638356E-16));
#8967=DIRECTION('',(0.,-1.,0.));
#8968=DIRECTION('',(-1.,0.,-1.92296268638356E-16));
#8969=DIRECTION('center_axis',(0.866025403784439,0.,0.5));
#8970=DIRECTION('ref_axis',(-0.5,0.,0.866025403784439));
#8971=DIRECTION('',(-0.5,0.,0.866025403784439));
#8972=DIRECTION('',(-0.5,0.,0.866025403784439));
#8973=DIRECTION('center_axis',(0.,-1.,0.));
#8974=DIRECTION('ref_axis',(0.,0.,-1.));
#8975=DIRECTION('center_axis',(0.,1.,0.));
#8976=DIRECTION('ref_axis',(0.,0.,1.));
#8977=DIRECTION('center_axis',(0.,-1.,0.));
#8978=DIRECTION('ref_axis',(1.,0.,0.));
#8979=DIRECTION('center_axis',(0.,-1.,0.));
#8980=DIRECTION('ref_axis',(1.,0.,0.));
#8981=DIRECTION('center_axis',(0.,-1.,0.));
#8982=DIRECTION('ref_axis',(1.,0.,0.));
#8983=DIRECTION('',(0.707106781186547,0.707106781186548,8.65956056235493E-17));
#8984=DIRECTION('center_axis',(0.,-1.,0.));
#8985=DIRECTION('ref_axis',(1.,0.,0.));
#8986=DIRECTION('center_axis',(0.,1.,0.));
#8987=DIRECTION('ref_axis',(1.,0.,0.));
#8988=DIRECTION('',(0.,1.,0.));
#8989=DIRECTION('center_axis',(0.,1.,0.));
#8990=DIRECTION('ref_axis',(1.,0.,0.));
#8991=DIRECTION('center_axis',(0.,-1.,0.));
#8992=DIRECTION('ref_axis',(1.,0.,0.));
#8993=DIRECTION('',(-0.707106781186547,0.707106781186548,-8.65956056235493E-17));
#8994=DIRECTION('center_axis',(0.,-1.,0.));
#8995=DIRECTION('ref_axis',(0.,0.,-1.));
#11505=CARTESIAN_POINT('',(0.,0.,0.));
#11506=CARTESIAN_POINT('Origin',(0.0721687836487032,0.,-0.125));
#11507=CARTESIAN_POINT('',(0.0721687836487032,0.,-0.125));
#11508=CARTESIAN_POINT('',(0.144337567297406,0.,0.));
#11509=CARTESIAN_POINT('',(0.117710979560879,0.,-0.0461186027918559));
#11510=CARTESIAN_POINT('',(0.0721687836487032,-0.25,-0.125));
#11511=CARTESIAN_POINT('',(0.0721687836487032,0.,-0.125));
#11512=CARTESIAN_POINT('',(0.144337567297406,-0.25,0.));
#11513=CARTESIAN_POINT('',(0.144337567297406,-0.25,0.));
#11514=CARTESIAN_POINT('',(0.144337567297406,0.,0.));
#11515=CARTESIAN_POINT('Origin',(-0.0721687836487032,0.,-0.125));
#11516=CARTESIAN_POINT('',(-0.0721687836487032,0.,-0.125));
#11517=CARTESIAN_POINT('',(0.0739156081756484,0.,-0.125));
#11518=CARTESIAN_POINT('',(-0.0721687836487032,-0.25,-0.125));
#11519=CARTESIAN_POINT('',(-0.0721687836487032,0.,-0.125));
#11520=CARTESIAN_POINT('',(0.0721687836487032,-0.25,-0.125));
#11521=CARTESIAN_POINT('Origin',(-0.144337567297406,0.,-4.16333634234434E-17));
#11522=CARTESIAN_POINT('',(-0.144337567297406,0.,-1.76762539787485E-17));
#11523=CARTESIAN_POINT('',(-0.0987953713852306,0.,-0.0788813972081442));
#11524=CARTESIAN_POINT('',(-0.144337567297406,-0.25,-2.77555756156289E-17));
#11525=CARTESIAN_POINT('',(-0.144337567297406,0.,-1.76762539787485E-17));
#11526=CARTESIAN_POINT('',(-0.0721687836487032,-0.25,-0.125));
#11527=CARTESIAN_POINT('Origin',(-0.0721687836487033,0.,0.125));
#11528=CARTESIAN_POINT('',(-0.0721687836487033,0.,0.125));
#11529=CARTESIAN_POINT('',(-0.0627109795608791,0.,0.141381397208144));
#11530=CARTESIAN_POINT('',(-0.0721687836487033,-0.25,0.125));
#11531=CARTESIAN_POINT('',(-0.0721687836487033,0.,0.125));
#11532=CARTESIAN_POINT('',(-0.144337567297406,-0.25,-1.76762539787485E-17));
#11533=CARTESIAN_POINT('Origin',(0.0721687836487032,0.,0.125));
#11534=CARTESIAN_POINT('',(0.0721687836487032,0.,0.125));
#11535=CARTESIAN_POINT('',(0.146084391824352,0.,0.125));
#11536=CARTESIAN_POINT('',(0.0721687836487032,-0.25,0.125));
#11537=CARTESIAN_POINT('',(0.0721687836487032,0.,0.125));
#11538=CARTESIAN_POINT('',(-0.0721687836487033,-0.25,0.125));
#11539=CARTESIAN_POINT('Origin',(0.144337567297406,0.,0.));
#11540=CARTESIAN_POINT('',(0.153795371385231,0.,-0.0163813972081441));
#11541=CARTESIAN_POINT('',(0.0721687836487032,-0.25,0.125));
#11542=CARTESIAN_POINT('Origin',(0.,-0.25,0.));
#11543=CARTESIAN_POINT('Origin',(0.22,0.,0.));
#11544=CARTESIAN_POINT('',(-0.22,-8.67361737988404E-18,-2.69422295812418E-17));
#11545=CARTESIAN_POINT('Origin',(0.,0.,0.));
#11546=CARTESIAN_POINT('Origin',(0.,-0.015,0.));
#11547=CARTESIAN_POINT('',(-0.24505,-0.02505,-3.00099698131059E-17));
#11548=CARTESIAN_POINT('Origin',(0.,-0.02505,0.));
#11549=CARTESIAN_POINT('',(-0.235,-0.015,-2.87791997799628E-17));
#11550=CARTESIAN_POINT('Origin',(0.,-0.3775,0.));
#11551=CARTESIAN_POINT('',(-0.24505,-0.72995,3.00099698131059E-17));
#11552=CARTESIAN_POINT('Origin',(0.,-0.72995,0.));
#11553=CARTESIAN_POINT('',(-0.24505,-0.3775,-3.00099698131059E-17));
#11554=CARTESIAN_POINT('Origin',(0.,-0.7625,0.));
#11555=CARTESIAN_POINT('',(-0.175,-0.8,-2.14313189850787E-17));
#11556=CARTESIAN_POINT('Origin',(0.,-0.8,0.));
#11557=CARTESIAN_POINT('',(-0.2125,-0.7625,-2.60237444818813E-17));
#11558=CARTESIAN_POINT('Origin',(0.,-0.8,0.));
#11757=UNCERTAINTY_MEASURE_WITH_UNIT(LENGTH_MEASURE(0.001),#11802,
'DISTANCE_ACCURACY_VALUE',
'Maximum model space distance between geometric entities at asserted c
onnectivities');
#11761=UNCERTAINTY_MEASURE_WITH_UNIT(LENGTH_MEASURE(0.001),#11802,
'DISTANCE_ACCURACY_VALUE',
'Maximum model space distance between geometric entities at asserted c
onnectivities');
#11797=(
GEOMETRIC_REPRESENTATION_CONTEXT(3)
GLOBAL_UNCERTAINTY_ASSIGNED_CONTEXT((#11757))
GLOBAL_UNIT_ASSIGNED_CONTEXT((#11802,#11804,#11805))
REPRESENTATION_CONTEXT('','3D')
);
#11801=(
GEOMETRIC_REPRESENTATION_CONTEXT(3)
GLOBAL_UNCERTAINTY_ASSIGNED_CONTEXT((#11761))
GLOBAL_UNIT_ASSIGNED_CONTEXT((#11802,#11804,#11805))
REPRESENTATION_CONTEXT('','3D')
);
#11802=(
LENGTH_UNIT()
NAMED_UNIT(*)
SI_UNIT(.CENTI.,.METRE.)
);
#11804=(
NAMED_UNIT(*)
PLANE_ANGLE_UNIT()
SI_UNIT($,.RADIAN.)
);
#11805=(
NAMED_UNIT(*)
SI_UNIT($,.STERADIAN.)
SOLID_ANGLE_UNIT()
);
#11841=SHAPE_DEFINITION_REPRESENTATION(#11882,#11980);
#11882=PRODUCT_DEFINITION_SHAPE('',$,#12020);
#11980=SHAPE_REPRESENTATION('',(#7243),#11797);
#11984=PRODUCT_DEFINITION_CONTEXT('part definition',#12103,'design');
#12020=PRODUCT_DEFINITION('Socket Set Screw - M5x8',
'Socket Set Screw - M5x8',#12059,#11984);
#12059=PRODUCT_DEFINITION_FORMATION('',$,#12140);
#12103=APPLICATION_CONTEXT(
'Core Data for Automotive Mechanical Design Process');
#12104=PRODUCT_CONTEXT('part definition',#12103,'mechanical');
#12140=PRODUCT('Socket Set Screw - M5x8','Socket Set Screw - M5x8',
'Socket Set Screw - M5x8',(#12104));
#12214=COLOUR_RGB('Black',0.12,0.14,0.17);
#12215=FILL_AREA_STYLE_COLOUR('',#12214);
#12216=FILL_AREA_STYLE('',(#12215));
#12217=SURFACE_STYLE_FILL_AREA(#12216);
#12218=SURFACE_SIDE_STYLE('',(#12217));
#12219=SURFACE_STYLE_USAGE(.BOTH.,#12218);
#12220=PRESENTATION_STYLE_ASSIGNMENT((#12219));
ENDSEC;
END-ISO-10303-21;
